ISO-10303-21;
HEADER;
/* Generated by software containing ST-Developer
 * from STEP Tools, Inc. (www.steptools.com) 
 */

FILE_DESCRIPTION(
/* description */ ('PAT-091'),
/* implementation_level */ '2;1');

FILE_NAME(
/* name */ 'Plain pivot bush (7).step',
/* time_stamp */ '2026-10-27T15:34:44-07:00',
/* author */ (''),
/* organization */ (''),
/* preprocessor_version */ 'ST-DEVELOPER v20.2',
/* originating_system */ 'Autodesk Translation Framework v15.17.0.0',
/* authorisation */ '');

FILE_SCHEMA (('AUTOMOTIVE_DESIGN { 1 0 10303 214 3 1 1 }'));
ENDSEC;

DATA;
#10=MECHANICAL_DESIGN_GEOMETRIC_PRESENTATION_REPRESENTATION('',(#1046),#25100);
#826=SHAPE_REPRESENTATION_RELATIONSHIP('SRR','None',#25593,#936);
#936=ADVANCED_BREP_SHAPE_REPRESENTATION('',(#1167),#25063);
#1046=STYLED_ITEM('',(#26177),#1167);
#1167=MANIFOLD_SOLID_BREP('Body1',#13326);
#1541=FACE_BOUND('',#3781,.T.);
#1542=FACE_BOUND('',#3783,.T.);
#1956=PLANE('',#15828);
#1957=PLANE('',#15829);
#2634=FACE_OUTER_BOUND('',#3778,.T.);
#2635=FACE_OUTER_BOUND('',#3779,.T.);
#2636=FACE_OUTER_BOUND('',#3780,.T.);
#2637=FACE_OUTER_BOUND('',#3782,.T.);
#3778=EDGE_LOOP('',(#11246,#11247,#11248,#11249));
#3779=EDGE_LOOP('',(#11250,#11251,#11252,#11253));
#3780=EDGE_LOOP('',(#11254));
#3781=EDGE_LOOP('',(#11255));
#3782=EDGE_LOOP('',(#11256));
#3783=EDGE_LOOP('',(#11257));
#4749=LINE('',#23650,#5489);
#4750=LINE('',#23656,#5490);
#5489=VECTOR('',#19571,0.605);
#5490=VECTOR('',#19578,1.);
#6112=CIRCLE('',#15823,0.605);
#6113=CIRCLE('',#15824,0.605);
#6114=CIRCLE('',#15826,1.);
#6115=CIRCLE('',#15827,1.);
#7137=VERTEX_POINT('',#23647);
#7138=VERTEX_POINT('',#23649);
#7139=VERTEX_POINT('',#23653);
#7140=VERTEX_POINT('',#23655);
#8558=EDGE_CURVE('',#7137,#7137,#6112,.T.);
#8559=EDGE_CURVE('',#7137,#7138,#4749,.T.);
#8560=EDGE_CURVE('',#7138,#7138,#6113,.T.);
#8561=EDGE_CURVE('',#7139,#7139,#6114,.T.);
#8562=EDGE_CURVE('',#7139,#7140,#4750,.T.);
#8563=EDGE_CURVE('',#7140,#7140,#6115,.T.);
#11246=ORIENTED_EDGE('',*,*,#8558,.F.);
#11247=ORIENTED_EDGE('',*,*,#8559,.T.);
#11248=ORIENTED_EDGE('',*,*,#8560,.T.);
#11249=ORIENTED_EDGE('',*,*,#8559,.F.);
#11250=ORIENTED_EDGE('',*,*,#8561,.F.);
#11251=ORIENTED_EDGE('',*,*,#8562,.T.);
#11252=ORIENTED_EDGE('',*,*,#8563,.T.);
#11253=ORIENTED_EDGE('',*,*,#8562,.F.);
#11254=ORIENTED_EDGE('',*,*,#8561,.T.);
#11255=ORIENTED_EDGE('',*,*,#8558,.T.);
#11256=ORIENTED_EDGE('',*,*,#8563,.F.);
#11257=ORIENTED_EDGE('',*,*,#8560,.F.);
#12317=CYLINDRICAL_SURFACE('',#15822,0.605);
#12318=CYLINDRICAL_SURFACE('',#15825,1.);
#13001=ADVANCED_FACE('',(#2634),#12317,.F.);
#13002=ADVANCED_FACE('',(#2635),#12318,.T.);
#13003=ADVANCED_FACE('',(#2636,#1541),#1956,.T.);
#13004=ADVANCED_FACE('',(#2637,#1542),#1957,.F.);
#13326=CLOSED_SHELL('',(#13001,#13002,#13003,#13004));
#15821=AXIS2_PLACEMENT_3D('',#23645,#19565,#19566);
#15822=AXIS2_PLACEMENT_3D('',#23646,#19567,#19568);
#15823=AXIS2_PLACEMENT_3D('',#23648,#19569,#19570);
#15824=AXIS2_PLACEMENT_3D('',#23651,#19572,#19573);
#15825=AXIS2_PLACEMENT_3D('',#23652,#19574,#19575);
#15826=AXIS2_PLACEMENT_3D('',#23654,#19576,#19577);
#15827=AXIS2_PLACEMENT_3D('',#23657,#19579,#19580);
#15828=AXIS2_PLACEMENT_3D('',#23658,#19581,#19582);
#15829=AXIS2_PLACEMENT_3D('',#23659,#19583,#19584);
#19565=DIRECTION('axis',(0.,0.,1.));
#19566=DIRECTION('refdir',(1.,0.,0.));
#19567=DIRECTION('center_axis',(0.,1.,0.));
#19568=DIRECTION('ref_axis',(1.,0.,0.));
#19569=DIRECTION('center_axis',(0.,-1.,0.));
#19570=DIRECTION('ref_axis',(1.,0.,0.));
#19571=DIRECTION('',(0.,-1.,0.));
#19572=DIRECTION('center_axis',(0.,-1.,0.));
#19573=DIRECTION('ref_axis',(1.,0.,0.));
#19574=DIRECTION('center_axis',(0.,1.,0.));
#19575=DIRECTION('ref_axis',(1.,0.,0.));
#19576=DIRECTION('center_axis',(0.,1.,0.));
#19577=DIRECTION('ref_axis',(1.,0.,0.));
#19578=DIRECTION('',(0.,-1.,0.));
#19579=DIRECTION('center_axis',(0.,1.,0.));
#19580=DIRECTION('ref_axis',(1.,0.,0.));
#19581=DIRECTION('center_axis',(0.,1.,0.));
#19582=DIRECTION('ref_axis',(1.,0.,0.));
#19583=DIRECTION('center_axis',(0.,1.,0.));
#19584=DIRECTION('ref_axis',(1.,0.,0.));
#23645=CARTESIAN_POINT('',(0.,0.,0.));
#23646=CARTESIAN_POINT('Origin',(0.,-5.5,13.));
#23647=CARTESIAN_POINT('',(-0.605,-4.5,13.));
#23648=CARTESIAN_POINT('Origin',(0.,-4.5,13.));
#23649=CARTESIAN_POINT('',(-0.605,-5.5,13.));
#23650=CARTESIAN_POINT('',(-0.605,-5.5,13.));
#23651=CARTESIAN_POINT('Origin',(0.,-5.5,13.));
#23652=CARTESIAN_POINT('Origin',(0.,-5.5,13.));
#23653=CARTESIAN_POINT('',(-1.,-4.5,13.));
#23654=CARTESIAN_POINT('Origin',(0.,-4.5,13.));
#23655=CARTESIAN_POINT('',(-1.,-5.5,13.));
#23656=CARTESIAN_POINT('',(-1.,-5.5,13.));
#23657=CARTESIAN_POINT('Origin',(0.,-5.5,13.));
#23658=CARTESIAN_POINT('Origin',(0.,-4.5,13.));
#23659=CARTESIAN_POINT('Origin',(0.,-5.5,13.));
#24942=UNCERTAINTY_MEASURE_WITH_UNIT(LENGTH_MEASURE(0.001),#25101,
'DISTANCE_ACCURACY_VALUE',
'Maximum model space distance between geometric entities at asserted c
onnectivities');
#24979=UNCERTAINTY_MEASURE_WITH_UNIT(LENGTH_MEASURE(0.001),#25101,
'DISTANCE_ACCURACY_VALUE',
'Maximum model space distance between geometric entities at asserted c
onnectivities');
#25063=(
GEOMETRIC_REPRESENTATION_CONTEXT(3)
GLOBAL_UNCERTAINTY_ASSIGNED_CONTEXT((#24942))
GLOBAL_UNIT_ASSIGNED_CONTEXT((#25101,#25103,#25104))
REPRESENTATION_CONTEXT('','3D')
);
#25100=(
GEOMETRIC_REPRESENTATION_CONTEXT(3)
GLOBAL_UNCERTAINTY_ASSIGNED_CONTEXT((#24979))
GLOBAL_UNIT_ASSIGNED_CONTEXT((#25101,#25103,#25104))
REPRESENTATION_CONTEXT('','3D')
);
#25101=(
LENGTH_UNIT()
NAMED_UNIT(*)
SI_UNIT(.CENTI.,.METRE.)
);
#25103=(
NAMED_UNIT(*)
PLANE_ANGLE_UNIT()
SI_UNIT($,.RADIAN.)
);
#25104=(
NAMED_UNIT(*)
SI_UNIT($,.STERADIAN.)
SOLID_ANGLE_UNIT()
);
#25188=SHAPE_DEFINITION_REPRESENTATION(#25382,#25593);
#25382=PRODUCT_DEFINITION_SHAPE('',$,#25714);
#25593=SHAPE_REPRESENTATION('',(#15821),#25063);
#25630=PRODUCT_DEFINITION_CONTEXT('part definition',#25992,'design');
#25714=PRODUCT_DEFINITION('Plain pivot bush (7)','Plain pivot bush (7)',#25834,
#25630);
#25834=PRODUCT_DEFINITION_FORMATION('',$,#26077);
#25992=APPLICATION_CONTEXT(
'Core Data for Automotive Mechanical Design Process');
#25993=PRODUCT_CONTEXT('part definition',#25992,'mechanical');
#26077=PRODUCT('Plain pivot bush (7)','Plain pivot bush (7)',
'Plain pivot bush (7)',(#25993));
#26171=COLOUR_RGB('Light Blue',0.38,0.62,0.78);
#26172=FILL_AREA_STYLE_COLOUR('',#26171);
#26173=FILL_AREA_STYLE('',(#26172));
#26174=SURFACE_STYLE_FILL_AREA(#26173);
#26175=SURFACE_SIDE_STYLE('',(#26174));
#26176=SURFACE_STYLE_USAGE(.BOTH.,#26175);
#26177=PRESENTATION_STYLE_ASSIGNMENT((#26176));
ENDSEC;
END-ISO-10303-21;
